ISO-10303-21;
HEADER;
/* Generated by software containing ST-Developer
 * from STEP Tools, Inc. (www.steptools.com) 
 */

FILE_DESCRIPTION(
/* description */ ('Over-Centre Plunger Toggle Clamp on Slotted Fixture Frame'),
/* implementation_level */ '2;1');

FILE_NAME(
/* name */ 
'Fixture foot strip (1).step',
/* time_stamp */ '2026-10-28T03:23:24-07:00',
/* author */ (''),
/* organization */ (''),
/* preprocessor_version */ 'ST-DEVELOPER v20.2',
/* originating_system */ 'Autodesk Translation Framework v15.17.0.0',
/* authorisation */ '');

FILE_SCHEMA (('AUTOMOTIVE_DESIGN { 1 0 10303 214 3 1 1 }'));
ENDSEC;

DATA;
#10=MECHANICAL_DESIGN_GEOMETRIC_PRESENTATION_REPRESENTATION('',(#516),#15212);
#432=SHAPE_REPRESENTATION_RELATIONSHIP('SRR','None',#15406,#474);
#474=ADVANCED_BREP_SHAPE_REPRESENTATION('',(#567),#15168);
#516=STYLED_ITEM('',(#15733),#567);
#567=MANIFOLD_SOLID_BREP('Body1',#8248);
#801=PLANE('',#8835);
#802=PLANE('',#8836);
#803=PLANE('',#8837);
#804=PLANE('',#8838);
#805=PLANE('',#8839);
#806=PLANE('',#8840);
#1121=FACE_OUTER_BOUND('',#1639,.T.);
#1122=FACE_OUTER_BOUND('',#1640,.T.);
#1123=FACE_OUTER_BOUND('',#1641,.T.);
#1124=FACE_OUTER_BOUND('',#1642,.T.);
#1125=FACE_OUTER_BOUND('',#1643,.T.);
#1126=FACE_OUTER_BOUND('',#1644,.T.);
#1639=EDGE_LOOP('',(#5737,#5738,#5739,#5740));
#1640=EDGE_LOOP('',(#5741,#5742,#5743,#5744));
#1641=EDGE_LOOP('',(#5745,#5746,#5747,#5748));
#1642=EDGE_LOOP('',(#5749,#5750,#5751,#5752));
#1643=EDGE_LOOP('',(#5753,#5754,#5755,#5756));
#1644=EDGE_LOOP('',(#5757,#5758,#5759,#5760));
#2283=LINE('',#12549,#2913);
#2284=LINE('',#12551,#2914);
#2285=LINE('',#12553,#2915);
#2286=LINE('',#12554,#2916);
#2287=LINE('',#12557,#2917);
#2288=LINE('',#12559,#2918);
#2289=LINE('',#12560,#2919);
#2290=LINE('',#12563,#2920);
#2291=LINE('',#12565,#2921);
#2292=LINE('',#12566,#2922);
#2293=LINE('',#12568,#2923);
#2294=LINE('',#12569,#2924);
#2913=VECTOR('',#9952,1.);
#2914=VECTOR('',#9953,1.);
#2915=VECTOR('',#9954,1.);
#2916=VECTOR('',#9955,1.);
#2917=VECTOR('',#9958,1.);
#2918=VECTOR('',#9959,1.);
#2919=VECTOR('',#9960,1.);
#2920=VECTOR('',#9963,1.);
#2921=VECTOR('',#9964,1.);
#2922=VECTOR('',#9965,1.);
#2923=VECTOR('',#9968,1.);
#2924=VECTOR('',#9969,1.);
#3915=VERTEX_POINT('',#12547);
#3916=VERTEX_POINT('',#12548);
#3917=VERTEX_POINT('',#12550);
#3918=VERTEX_POINT('',#12552);
#3919=VERTEX_POINT('',#12556);
#3920=VERTEX_POINT('',#12558);
#3921=VERTEX_POINT('',#12562);
#3922=VERTEX_POINT('',#12564);
#4629=EDGE_CURVE('',#3915,#3916,#2283,.T.);
#4630=EDGE_CURVE('',#3916,#3917,#2284,.T.);
#4631=EDGE_CURVE('',#3918,#3917,#2285,.T.);
#4632=EDGE_CURVE('',#3915,#3918,#2286,.T.);
#4633=EDGE_CURVE('',#3919,#3915,#2287,.T.);
#4634=EDGE_CURVE('',#3920,#3918,#2288,.T.);
#4635=EDGE_CURVE('',#3919,#3920,#2289,.T.);
#4636=EDGE_CURVE('',#3921,#3919,#2290,.T.);
#4637=EDGE_CURVE('',#3922,#3920,#2291,.T.);
#4638=EDGE_CURVE('',#3921,#3922,#2292,.T.);
#4639=EDGE_CURVE('',#3916,#3921,#2293,.T.);
#4640=EDGE_CURVE('',#3917,#3922,#2294,.T.);
#5737=ORIENTED_EDGE('',*,*,#4629,.T.);
#5738=ORIENTED_EDGE('',*,*,#4630,.T.);
#5739=ORIENTED_EDGE('',*,*,#4631,.F.);
#5740=ORIENTED_EDGE('',*,*,#4632,.F.);
#5741=ORIENTED_EDGE('',*,*,#4633,.T.);
#5742=ORIENTED_EDGE('',*,*,#4632,.T.);
#5743=ORIENTED_EDGE('',*,*,#4634,.F.);
#5744=ORIENTED_EDGE('',*,*,#4635,.F.);
#5745=ORIENTED_EDGE('',*,*,#4636,.T.);
#5746=ORIENTED_EDGE('',*,*,#4635,.T.);
#5747=ORIENTED_EDGE('',*,*,#4637,.F.);
#5748=ORIENTED_EDGE('',*,*,#4638,.F.);
#5749=ORIENTED_EDGE('',*,*,#4639,.T.);
#5750=ORIENTED_EDGE('',*,*,#4638,.T.);
#5751=ORIENTED_EDGE('',*,*,#4640,.F.);
#5752=ORIENTED_EDGE('',*,*,#4630,.F.);
#5753=ORIENTED_EDGE('',*,*,#4640,.T.);
#5754=ORIENTED_EDGE('',*,*,#4637,.T.);
#5755=ORIENTED_EDGE('',*,*,#4634,.T.);
#5756=ORIENTED_EDGE('',*,*,#4631,.T.);
#5757=ORIENTED_EDGE('',*,*,#4639,.F.);
#5758=ORIENTED_EDGE('',*,*,#4629,.F.);
#5759=ORIENTED_EDGE('',*,*,#4633,.F.);
#5760=ORIENTED_EDGE('',*,*,#4636,.F.);
#7793=ADVANCED_FACE('',(#1121),#801,.T.);
#7794=ADVANCED_FACE('',(#1122),#802,.T.);
#7795=ADVANCED_FACE('',(#1123),#803,.T.);
#7796=ADVANCED_FACE('',(#1124),#804,.T.);
#7797=ADVANCED_FACE('',(#1125),#805,.T.);
#7798=ADVANCED_FACE('',(#1126),#806,.F.);
#8248=CLOSED_SHELL('',(#7793,#7794,#7795,#7796,#7797,#7798));
#8834=AXIS2_PLACEMENT_3D('',#12545,#9948,#9949);
#8835=AXIS2_PLACEMENT_3D('',#12546,#9950,#9951);
#8836=AXIS2_PLACEMENT_3D('',#12555,#9956,#9957);
#8837=AXIS2_PLACEMENT_3D('',#12561,#9961,#9962);
#8838=AXIS2_PLACEMENT_3D('',#12567,#9966,#9967);
#8839=AXIS2_PLACEMENT_3D('',#12570,#9970,#9971);
#8840=AXIS2_PLACEMENT_3D('',#12571,#9972,#9973);
#9948=DIRECTION('axis',(0.,0.,1.));
#9949=DIRECTION('refdir',(1.,0.,0.));
#9950=DIRECTION('center_axis',(0.,1.,0.));
#9951=DIRECTION('ref_axis',(-1.,0.,0.));
#9952=DIRECTION('',(-1.,0.,0.));
#9953=DIRECTION('',(0.,0.,1.));
#9954=DIRECTION('',(-1.,0.,0.));
#9955=DIRECTION('',(0.,0.,1.));
#9956=DIRECTION('center_axis',(1.,0.,0.));
#9957=DIRECTION('ref_axis',(0.,1.,0.));
#9958=DIRECTION('',(0.,1.,0.));
#9959=DIRECTION('',(0.,1.,0.));
#9960=DIRECTION('',(0.,0.,1.));
#9961=DIRECTION('center_axis',(0.,-1.,0.));
#9962=DIRECTION('ref_axis',(1.,0.,0.));
#9963=DIRECTION('',(1.,0.,0.));
#9964=DIRECTION('',(1.,0.,0.));
#9965=DIRECTION('',(0.,0.,1.));
#9966=DIRECTION('center_axis',(-1.,0.,0.));
#9967=DIRECTION('ref_axis',(0.,-1.,0.));
#9968=DIRECTION('',(0.,-1.,0.));
#9969=DIRECTION('',(0.,-1.,0.));
#9970=DIRECTION('center_axis',(0.,0.,1.));
#9971=DIRECTION('ref_axis',(1.,0.,0.));
#9972=DIRECTION('center_axis',(0.,0.,1.));
#9973=DIRECTION('ref_axis',(1.,0.,0.));
#12545=CARTESIAN_POINT('',(0.,0.,0.));
#12546=CARTESIAN_POINT('Origin',(10.5,4.5,-3.6));
#12547=CARTESIAN_POINT('',(10.5,4.5,-3.6));
#12548=CARTESIAN_POINT('',(9.5,4.5,-3.6));
#12549=CARTESIAN_POINT('',(10.5,4.5,-3.6));
#12550=CARTESIAN_POINT('',(9.5,4.5,-2.8));
#12551=CARTESIAN_POINT('',(9.5,4.5,-3.6));
#12552=CARTESIAN_POINT('',(10.5,4.5,-2.8));
#12553=CARTESIAN_POINT('',(10.5,4.5,-2.8));
#12554=CARTESIAN_POINT('',(10.5,4.5,-3.6));
#12555=CARTESIAN_POINT('Origin',(10.5,-7.,-3.6));
#12556=CARTESIAN_POINT('',(10.5,-7.,-3.6));
#12557=CARTESIAN_POINT('',(10.5,-7.,-3.6));
#12558=CARTESIAN_POINT('',(10.5,-7.,-2.8));
#12559=CARTESIAN_POINT('',(10.5,-7.,-2.8));
#12560=CARTESIAN_POINT('',(10.5,-7.,-3.6));
#12561=CARTESIAN_POINT('Origin',(9.5,-7.,-3.6));
#12562=CARTESIAN_POINT('',(9.5,-7.,-3.6));
#12563=CARTESIAN_POINT('',(9.5,-7.,-3.6));
#12564=CARTESIAN_POINT('',(9.5,-7.,-2.8));
#12565=CARTESIAN_POINT('',(9.5,-7.,-2.8));
#12566=CARTESIAN_POINT('',(9.5,-7.,-3.6));
#12567=CARTESIAN_POINT('Origin',(9.5,4.5,-3.6));
#12568=CARTESIAN_POINT('',(9.5,4.5,-3.6));
#12569=CARTESIAN_POINT('',(9.5,4.5,-2.8));
#12570=CARTESIAN_POINT('Origin',(10.,-1.25,-2.8));
#12571=CARTESIAN_POINT('Origin',(10.,-1.25,-3.6));
#15118=UNCERTAINTY_MEASURE_WITH_UNIT(LENGTH_MEASURE(0.001),#15213,
'DISTANCE_ACCURACY_VALUE',
'Maximum model space distance between geometric entities at asserted c
onnectivities');
#15162=UNCERTAINTY_MEASURE_WITH_UNIT(LENGTH_MEASURE(0.001),#15213,
'DISTANCE_ACCURACY_VALUE',
'Maximum model space distance between geometric entities at asserted c
onnectivities');
#15168=(
GEOMETRIC_REPRESENTATION_CONTEXT(3)
GLOBAL_UNCERTAINTY_ASSIGNED_CONTEXT((#15118))
GLOBAL_UNIT_ASSIGNED_CONTEXT((#15213,#15215,#15216))
REPRESENTATION_CONTEXT('','3D')
);
#15212=(
GEOMETRIC_REPRESENTATION_CONTEXT(3)
GLOBAL_UNCERTAINTY_ASSIGNED_CONTEXT((#15162))
GLOBAL_UNIT_ASSIGNED_CONTEXT((#15213,#15215,#15216))
REPRESENTATION_CONTEXT('','3D')
);
#15213=(
LENGTH_UNIT()
NAMED_UNIT(*)
SI_UNIT(.CENTI.,.METRE.)
);
#15215=(
NAMED_UNIT(*)
PLANE_ANGLE_UNIT()
SI_UNIT($,.RADIAN.)
);
#15216=(
NAMED_UNIT(*)
SI_UNIT($,.STERADIAN.)
SOLID_ANGLE_UNIT()
);
#15222=SHAPE_DEFINITION_REPRESENTATION(#15271,#15406);
#15271=PRODUCT_DEFINITION_SHAPE('',$,#15456);
#15406=SHAPE_REPRESENTATION('',(#8834),#15168);
#15450=PRODUCT_DEFINITION_CONTEXT('part definition',#15599,'design');
#15456=PRODUCT_DEFINITION('Fixture foot strip (1)',
'Fixture foot strip (1)',#15505,#15450);
#15505=PRODUCT_DEFINITION_FORMATION('',$,#15606);
#15599=APPLICATION_CONTEXT(
'Core Data for Automotive Mechanical Design Process');
#15600=PRODUCT_CONTEXT('part definition',#15599,'mechanical');
#15606=PRODUCT('Fixture foot strip (1)','Fixture foot strip (1)',
'Fixture foot strip (1)',(#15600));
#15727=COLOUR_RGB('Off White',0.89,0.88,0.83);
#15728=FILL_AREA_STYLE_COLOUR('',#15727);
#15729=FILL_AREA_STYLE('',(#15728));
#15730=SURFACE_STYLE_FILL_AREA(#15729);
#15731=SURFACE_SIDE_STYLE('',(#15730));
#15732=SURFACE_STYLE_USAGE(.BOTH.,#15731);
#15733=PRESENTATION_STYLE_ASSIGNMENT((#15732));
ENDSEC;
END-ISO-10303-21;
